ISO-10303-21;
HEADER;
/* Generated by software containing ST-Developer
 * from STEP Tools, Inc. (www.steptools.com) 
 */

FILE_DESCRIPTION(
/* description */ ('PAT-082'),
/* implementation_level */ '2;1');

FILE_NAME(
/* name */ 'Blanking plug.step',
/* time_stamp */ '2026-10-29T20:16:13-07:00',
/* author */ (''),
/* organization */ (''),
/* preprocessor_version */ 'ST-DEVELOPER v20.2',
/* originating_system */ 'Autodesk Translation Framework v15.17.0.0',
/* authorisation */ '');

FILE_SCHEMA (('AUTOMOTIVE_DESIGN { 1 0 10303 214 3 1 1 }'));
ENDSEC;

DATA;
#10=MECHANICAL_DESIGN_GEOMETRIC_PRESENTATION_REPRESENTATION('',(#253),#8266);
#209=SHAPE_REPRESENTATION_RELATIONSHIP('SRR','None',#8371,#231);
#231=ADVANCED_BREP_SHAPE_REPRESENTATION('',(#275),#8255);
#253=STYLED_ITEM('',(#8551),#275);
#275=MANIFOLD_SOLID_BREP('Body1',#4593);
#384=FACE_BOUND('',#1104,.T.);
#495=PLANE('',#5166);
#496=PLANE('',#5168);
#497=PLANE('',#5169);
#498=PLANE('',#5170);
#499=PLANE('',#5171);
#500=PLANE('',#5172);
#501=PLANE('',#5173);
#502=PLANE('',#5174);
#503=PLANE('',#5177);
#731=FACE_OUTER_BOUND('',#1103,.T.);
#732=FACE_OUTER_BOUND('',#1105,.T.);
#733=FACE_OUTER_BOUND('',#1106,.T.);
#734=FACE_OUTER_BOUND('',#1107,.T.);
#735=FACE_OUTER_BOUND('',#1108,.T.);
#736=FACE_OUTER_BOUND('',#1109,.T.);
#737=FACE_OUTER_BOUND('',#1110,.T.);
#738=FACE_OUTER_BOUND('',#1111,.T.);
#739=FACE_OUTER_BOUND('',#1112,.T.);
#740=FACE_OUTER_BOUND('',#1113,.T.);
#1103=EDGE_LOOP('',(#3800,#3801,#3802,#3803,#3804,#3805));
#1104=EDGE_LOOP('',(#3806));
#1105=EDGE_LOOP('',(#3807,#3808,#3809,#3810));
#1106=EDGE_LOOP('',(#3811,#3812,#3813,#3814));
#1107=EDGE_LOOP('',(#3815,#3816,#3817,#3818));
#1108=EDGE_LOOP('',(#3819,#3820,#3821,#3822));
#1109=EDGE_LOOP('',(#3823,#3824,#3825,#3826));
#1110=EDGE_LOOP('',(#3827,#3828,#3829,#3830));
#1111=EDGE_LOOP('',(#3831,#3832,#3833,#3834,#3835,#3836));
#1112=EDGE_LOOP('',(#3837,#3838,#3839,#3840));
#1113=EDGE_LOOP('',(#3841));
#1436=LINE('',#7714,#1791);
#1437=LINE('',#7716,#1792);
#1438=LINE('',#7718,#1793);
#1439=LINE('',#7720,#1794);
#1440=LINE('',#7722,#1795);
#1441=LINE('',#7723,#1796);
#1442=LINE('',#7728,#1797);
#1443=LINE('',#7730,#1798);
#1444=LINE('',#7731,#1799);
#1445=LINE('',#7734,#1800);
#1446=LINE('',#7735,#1801);
#1447=LINE('',#7738,#1802);
#1448=LINE('',#7739,#1803);
#1449=LINE('',#7742,#1804);
#1450=LINE('',#7743,#1805);
#1451=LINE('',#7746,#1806);
#1452=LINE('',#7747,#1807);
#1453=LINE('',#7749,#1808);
#1454=LINE('',#7753,#1809);
#1791=VECTOR('',#6219,1.);
#1792=VECTOR('',#6220,1.);
#1793=VECTOR('',#6221,1.);
#1794=VECTOR('',#6222,1.);
#1795=VECTOR('',#6223,1.);
#1796=VECTOR('',#6224,1.);
#1797=VECTOR('',#6229,1.);
#1798=VECTOR('',#6230,1.);
#1799=VECTOR('',#6231,1.);
#1800=VECTOR('',#6234,1.);
#1801=VECTOR('',#6235,1.);
#1802=VECTOR('',#6238,1.);
#1803=VECTOR('',#6239,1.);
#1804=VECTOR('',#6242,1.);
#1805=VECTOR('',#6243,1.);
#1806=VECTOR('',#6246,1.);
#1807=VECTOR('',#6247,1.);
#1808=VECTOR('',#6250,1.);
#1809=VECTOR('',#6255,0.685);
#2089=CIRCLE('',#5167,0.685);
#2090=CIRCLE('',#5176,0.685);
#2383=VERTEX_POINT('',#7712);
#2384=VERTEX_POINT('',#7713);
#2385=VERTEX_POINT('',#7715);
#2386=VERTEX_POINT('',#7717);
#2387=VERTEX_POINT('',#7719);
#2388=VERTEX_POINT('',#7721);
#2389=VERTEX_POINT('',#7724);
#2390=VERTEX_POINT('',#7727);
#2391=VERTEX_POINT('',#7729);
#2392=VERTEX_POINT('',#7733);
#2393=VERTEX_POINT('',#7737);
#2394=VERTEX_POINT('',#7741);
#2395=VERTEX_POINT('',#7745);
#2396=VERTEX_POINT('',#7752);
#2876=EDGE_CURVE('',#2383,#2384,#1436,.T.);
#2877=EDGE_CURVE('',#2385,#2383,#1437,.T.);
#2878=EDGE_CURVE('',#2386,#2385,#1438,.T.);
#2879=EDGE_CURVE('',#2387,#2386,#1439,.T.);
#2880=EDGE_CURVE('',#2388,#2387,#1440,.T.);
#2881=EDGE_CURVE('',#2384,#2388,#1441,.T.);
#2882=EDGE_CURVE('',#2389,#2389,#2089,.T.);
#2883=EDGE_CURVE('',#2383,#2390,#1442,.T.);
#2884=EDGE_CURVE('',#2391,#2390,#1443,.T.);
#2885=EDGE_CURVE('',#2385,#2391,#1444,.T.);
#2886=EDGE_CURVE('',#2392,#2391,#1445,.T.);
#2887=EDGE_CURVE('',#2386,#2392,#1446,.T.);
#2888=EDGE_CURVE('',#2393,#2392,#1447,.T.);
#2889=EDGE_CURVE('',#2387,#2393,#1448,.T.);
#2890=EDGE_CURVE('',#2394,#2393,#1449,.T.);
#2891=EDGE_CURVE('',#2388,#2394,#1450,.T.);
#2892=EDGE_CURVE('',#2395,#2394,#1451,.T.);
#2893=EDGE_CURVE('',#2384,#2395,#1452,.T.);
#2894=EDGE_CURVE('',#2390,#2395,#1453,.T.);
#2895=EDGE_CURVE('',#2389,#2396,#1454,.T.);
#2896=EDGE_CURVE('',#2396,#2396,#2090,.T.);
#3800=ORIENTED_EDGE('',*,*,#2876,.F.);
#3801=ORIENTED_EDGE('',*,*,#2877,.F.);
#3802=ORIENTED_EDGE('',*,*,#2878,.F.);
#3803=ORIENTED_EDGE('',*,*,#2879,.F.);
#3804=ORIENTED_EDGE('',*,*,#2880,.F.);
#3805=ORIENTED_EDGE('',*,*,#2881,.F.);
#3806=ORIENTED_EDGE('',*,*,#2882,.T.);
#3807=ORIENTED_EDGE('',*,*,#2877,.T.);
#3808=ORIENTED_EDGE('',*,*,#2883,.T.);
#3809=ORIENTED_EDGE('',*,*,#2884,.F.);
#3810=ORIENTED_EDGE('',*,*,#2885,.F.);
#3811=ORIENTED_EDGE('',*,*,#2878,.T.);
#3812=ORIENTED_EDGE('',*,*,#2885,.T.);
#3813=ORIENTED_EDGE('',*,*,#2886,.F.);
#3814=ORIENTED_EDGE('',*,*,#2887,.F.);
#3815=ORIENTED_EDGE('',*,*,#2879,.T.);
#3816=ORIENTED_EDGE('',*,*,#2887,.T.);
#3817=ORIENTED_EDGE('',*,*,#2888,.F.);
#3818=ORIENTED_EDGE('',*,*,#2889,.F.);
#3819=ORIENTED_EDGE('',*,*,#2880,.T.);
#3820=ORIENTED_EDGE('',*,*,#2889,.T.);
#3821=ORIENTED_EDGE('',*,*,#2890,.F.);
#3822=ORIENTED_EDGE('',*,*,#2891,.F.);
#3823=ORIENTED_EDGE('',*,*,#2881,.T.);
#3824=ORIENTED_EDGE('',*,*,#2891,.T.);
#3825=ORIENTED_EDGE('',*,*,#2892,.F.);
#3826=ORIENTED_EDGE('',*,*,#2893,.F.);
#3827=ORIENTED_EDGE('',*,*,#2876,.T.);
#3828=ORIENTED_EDGE('',*,*,#2893,.T.);
#3829=ORIENTED_EDGE('',*,*,#2894,.F.);
#3830=ORIENTED_EDGE('',*,*,#2883,.F.);
#3831=ORIENTED_EDGE('',*,*,#2894,.T.);
#3832=ORIENTED_EDGE('',*,*,#2892,.T.);
#3833=ORIENTED_EDGE('',*,*,#2890,.T.);
#3834=ORIENTED_EDGE('',*,*,#2888,.T.);
#3835=ORIENTED_EDGE('',*,*,#2886,.T.);
#3836=ORIENTED_EDGE('',*,*,#2884,.T.);
#3837=ORIENTED_EDGE('',*,*,#2882,.F.);
#3838=ORIENTED_EDGE('',*,*,#2895,.T.);
#3839=ORIENTED_EDGE('',*,*,#2896,.T.);
#3840=ORIENTED_EDGE('',*,*,#2895,.F.);
#3841=ORIENTED_EDGE('',*,*,#2896,.F.);
#4289=CYLINDRICAL_SURFACE('',#5175,0.685);
#4470=ADVANCED_FACE('',(#731,#384),#495,.F.);
#4471=ADVANCED_FACE('',(#732),#496,.T.);
#4472=ADVANCED_FACE('',(#733),#497,.T.);
#4473=ADVANCED_FACE('',(#734),#498,.T.);
#4474=ADVANCED_FACE('',(#735),#499,.T.);
#4475=ADVANCED_FACE('',(#736),#500,.T.);
#4476=ADVANCED_FACE('',(#737),#501,.T.);
#4477=ADVANCED_FACE('',(#738),#502,.T.);
#4478=ADVANCED_FACE('',(#739),#4289,.T.);
#4479=ADVANCED_FACE('',(#740),#503,.F.);
#4593=CLOSED_SHELL('',(#4470,#4471,#4472,#4473,#4474,#4475,#4476,#4477,
#4478,#4479));
#5165=AXIS2_PLACEMENT_3D('',#7710,#6215,#6216);
#5166=AXIS2_PLACEMENT_3D('',#7711,#6217,#6218);
#5167=AXIS2_PLACEMENT_3D('',#7725,#6225,#6226);
#5168=AXIS2_PLACEMENT_3D('',#7726,#6227,#6228);
#5169=AXIS2_PLACEMENT_3D('',#7732,#6232,#6233);
#5170=AXIS2_PLACEMENT_3D('',#7736,#6236,#6237);
#5171=AXIS2_PLACEMENT_3D('',#7740,#6240,#6241);
#5172=AXIS2_PLACEMENT_3D('',#7744,#6244,#6245);
#5173=AXIS2_PLACEMENT_3D('',#7748,#6248,#6249);
#5174=AXIS2_PLACEMENT_3D('',#7750,#6251,#6252);
#5175=AXIS2_PLACEMENT_3D('',#7751,#6253,#6254);
#5176=AXIS2_PLACEMENT_3D('',#7754,#6256,#6257);
#5177=AXIS2_PLACEMENT_3D('',#7755,#6258,#6259);
#6215=DIRECTION('axis',(0.,0.,1.));
#6216=DIRECTION('refdir',(1.,0.,0.));
#6217=DIRECTION('center_axis',(1.,0.,0.));
#6218=DIRECTION('ref_axis',(0.,0.,-1.));
#6219=DIRECTION('',(0.,0.5,0.866025403784439));
#6220=DIRECTION('',(0.,1.,-4.39534328316243E-16));
#6221=DIRECTION('',(0.,0.5,-0.866025403784439));
#6222=DIRECTION('',(0.,-0.5,-0.866025403784439));
#6223=DIRECTION('',(0.,-1.,0.));
#6224=DIRECTION('',(0.,-0.5,0.866025403784439));
#6225=DIRECTION('center_axis',(1.,0.,0.));
#6226=DIRECTION('ref_axis',(0.,0.,-1.));
#6227=DIRECTION('center_axis',(0.,-4.39534328316243E-16,-1.));
#6228=DIRECTION('ref_axis',(0.,1.,-4.39534328316243E-16));
#6229=DIRECTION('',(1.,0.,0.));
#6230=DIRECTION('',(0.,1.,-4.39534328316243E-16));
#6231=DIRECTION('',(1.,0.,0.));
#6232=DIRECTION('center_axis',(0.,-0.866025403784439,-0.5));
#6233=DIRECTION('ref_axis',(0.,0.5,-0.866025403784439));
#6234=DIRECTION('',(0.,0.5,-0.866025403784439));
#6235=DIRECTION('',(1.,0.,0.));
#6236=DIRECTION('center_axis',(0.,-0.866025403784439,0.5));
#6237=DIRECTION('ref_axis',(0.,-0.5,-0.866025403784439));
#6238=DIRECTION('',(0.,-0.5,-0.866025403784439));
#6239=DIRECTION('',(1.,0.,0.));
#6240=DIRECTION('center_axis',(0.,0.,1.));
#6241=DIRECTION('ref_axis',(0.,-1.,0.));
#6242=DIRECTION('',(0.,-1.,0.));
#6243=DIRECTION('',(1.,0.,0.));
#6244=DIRECTION('center_axis',(0.,0.866025403784439,0.5));
#6245=DIRECTION('ref_axis',(0.,-0.5,0.866025403784439));
#6246=DIRECTION('',(0.,-0.5,0.866025403784439));
#6247=DIRECTION('',(1.,0.,0.));
#6248=DIRECTION('center_axis',(0.,0.866025403784439,-0.5));
#6249=DIRECTION('ref_axis',(0.,0.5,0.866025403784439));
#6250=DIRECTION('',(0.,0.5,0.866025403784439));
#6251=DIRECTION('center_axis',(1.,0.,0.));
#6252=DIRECTION('ref_axis',(0.,0.,-1.));
#6253=DIRECTION('center_axis',(1.,0.,0.));
#6254=DIRECTION('ref_axis',(0.,0.,-1.));
#6255=DIRECTION('',(-1.,0.,0.));
#6256=DIRECTION('center_axis',(1.,0.,0.));
#6257=DIRECTION('ref_axis',(0.,0.,-1.));
#6258=DIRECTION('center_axis',(1.,0.,0.));
#6259=DIRECTION('ref_axis',(0.,0.,-1.));
#7710=CARTESIAN_POINT('',(0.,0.,0.));
#7711=CARTESIAN_POINT('Origin',(5.5,0.,3.5));
#7712=CARTESIAN_POINT('',(5.5,0.505181485540923,2.625));
#7713=CARTESIAN_POINT('',(5.5,1.01036297108185,3.5));
#7714=CARTESIAN_POINT('',(5.5,0.505181485540923,2.625));
#7715=CARTESIAN_POINT('',(5.5,-0.505181485540923,2.625));
#7716=CARTESIAN_POINT('',(5.5,-0.505181485540923,2.625));
#7717=CARTESIAN_POINT('',(5.5,-1.01036297108185,3.5));
#7718=CARTESIAN_POINT('',(5.5,-1.01036297108185,3.5));
#7719=CARTESIAN_POINT('',(5.5,-0.505181485540922,4.375));
#7720=CARTESIAN_POINT('',(5.5,-0.505181485540922,4.375));
#7721=CARTESIAN_POINT('',(5.5,0.505181485540923,4.375));
#7722=CARTESIAN_POINT('',(5.5,0.505181485540923,4.375));
#7723=CARTESIAN_POINT('',(5.5,1.01036297108185,3.5));
#7724=CARTESIAN_POINT('',(5.5,-8.38883057415937E-17,4.185));
#7725=CARTESIAN_POINT('Origin',(5.5,0.,3.5));
#7726=CARTESIAN_POINT('Origin',(5.5,-0.505181485540923,2.625));
#7727=CARTESIAN_POINT('',(6.1,0.505181485540923,2.625));
#7728=CARTESIAN_POINT('',(5.5,0.505181485540923,2.625));
#7729=CARTESIAN_POINT('',(6.1,-0.505181485540923,2.625));
#7730=CARTESIAN_POINT('',(6.1,-0.505181485540923,2.625));
#7731=CARTESIAN_POINT('',(5.5,-0.505181485540923,2.625));
#7732=CARTESIAN_POINT('Origin',(5.5,-1.01036297108185,3.5));
#7733=CARTESIAN_POINT('',(6.1,-1.01036297108185,3.5));
#7734=CARTESIAN_POINT('',(6.1,-1.01036297108185,3.5));
#7735=CARTESIAN_POINT('',(5.5,-1.01036297108185,3.5));
#7736=CARTESIAN_POINT('Origin',(5.5,-0.505181485540922,4.375));
#7737=CARTESIAN_POINT('',(6.1,-0.505181485540922,4.375));
#7738=CARTESIAN_POINT('',(6.1,-0.505181485540922,4.375));
#7739=CARTESIAN_POINT('',(5.5,-0.505181485540922,4.375));
#7740=CARTESIAN_POINT('Origin',(5.5,0.505181485540923,4.375));
#7741=CARTESIAN_POINT('',(6.1,0.505181485540923,4.375));
#7742=CARTESIAN_POINT('',(6.1,0.505181485540923,4.375));
#7743=CARTESIAN_POINT('',(5.5,0.505181485540923,4.375));
#7744=CARTESIAN_POINT('Origin',(5.5,1.01036297108185,3.5));
#7745=CARTESIAN_POINT('',(6.1,1.01036297108185,3.5));
#7746=CARTESIAN_POINT('',(6.1,1.01036297108185,3.5));
#7747=CARTESIAN_POINT('',(5.5,1.01036297108185,3.5));
#7748=CARTESIAN_POINT('Origin',(5.5,0.505181485540923,2.625));
#7749=CARTESIAN_POINT('',(6.1,0.505181485540923,2.625));
#7750=CARTESIAN_POINT('Origin',(6.1,0.,3.5));
#7751=CARTESIAN_POINT('Origin',(4.1,0.,3.5));
#7752=CARTESIAN_POINT('',(4.1,-8.38883057415937E-17,4.185));
#7753=CARTESIAN_POINT('',(4.1,-8.38883057415937E-17,4.185));
#7754=CARTESIAN_POINT('Origin',(4.1,0.,3.5));
#7755=CARTESIAN_POINT('Origin',(4.1,0.,3.5));
#8230=UNCERTAINTY_MEASURE_WITH_UNIT(LENGTH_MEASURE(0.001),#8267,
'DISTANCE_ACCURACY_VALUE',
'Maximum model space distance between geometric entities at asserted c
onnectivities');
#8241=UNCERTAINTY_MEASURE_WITH_UNIT(LENGTH_MEASURE(0.001),#8267,
'DISTANCE_ACCURACY_VALUE',
'Maximum model space distance between geometric entities at asserted c
onnectivities');
#8255=(
GEOMETRIC_REPRESENTATION_CONTEXT(3)
GLOBAL_UNCERTAINTY_ASSIGNED_CONTEXT((#8230))
GLOBAL_UNIT_ASSIGNED_CONTEXT((#8267,#8269,#8270))
REPRESENTATION_CONTEXT('','3D')
);
#8266=(
GEOMETRIC_REPRESENTATION_CONTEXT(3)
GLOBAL_UNCERTAINTY_ASSIGNED_CONTEXT((#8241))
GLOBAL_UNIT_ASSIGNED_CONTEXT((#8267,#8269,#8270))
REPRESENTATION_CONTEXT('','3D')
);
#8267=(
LENGTH_UNIT()
NAMED_UNIT(*)
SI_UNIT(.CENTI.,.METRE.)
);
#8269=(
NAMED_UNIT(*)
PLANE_ANGLE_UNIT()
SI_UNIT($,.RADIAN.)
);
#8270=(
NAMED_UNIT(*)
SI_UNIT($,.STERADIAN.)
SOLID_ANGLE_UNIT()
);
#8284=SHAPE_DEFINITION_REPRESENTATION(#8308,#8371);
#8308=PRODUCT_DEFINITION_SHAPE('',$,#8396);
#8371=SHAPE_REPRESENTATION('',(#5165),#8255);
#8382=PRODUCT_DEFINITION_CONTEXT('part definition',#8456,'design');
#8396=PRODUCT_DEFINITION('Blanking plug','Blanking plug',#8420,
#8382);
#8420=PRODUCT_DEFINITION_FORMATION('',$,#8471);
#8456=APPLICATION_CONTEXT(
'Core Data for Automotive Mechanical Design Process');
#8457=PRODUCT_CONTEXT('part definition',#8456,'mechanical');
#8471=PRODUCT('Blanking plug','Blanking plug','Blanking plug',
(#8457));
#8545=COLOUR_RGB('Off White',0.89,0.88,0.83);
#8546=FILL_AREA_STYLE_COLOUR('',#8545);
#8547=FILL_AREA_STYLE('',(#8546));
#8548=SURFACE_STYLE_FILL_AREA(#8547);
#8549=SURFACE_SIDE_STYLE('',(#8548));
#8550=SURFACE_STYLE_USAGE(.BOTH.,#8549);
#8551=PRESENTATION_STYLE_ASSIGNMENT((#8550));
ENDSEC;
END-ISO-10303-21;
